ISO-10303-21;
HEADER;
/* Generated by software containing ST-Developer
 * from STEP Tools, Inc. (www.steptools.com) 
 */

FILE_DESCRIPTION(
/* description */ ('Bin tilter linkage'),
/* implementation_level */ '2;1');

FILE_NAME(
/* name */ 'M4 short cap screw (1).step',
/* time_stamp */ '2026-10-28T03:26:24-07:00',
/* author */ (''),
/* organization */ (''),
/* preprocessor_version */ 'ST-DEVELOPER v20.2',
/* originating_system */ 'Autodesk Translation Framework v15.17.0.0',
/* authorisation */ '');

FILE_SCHEMA (('AUTOMOTIVE_DESIGN { 1 0 10303 214 3 1 1 }'));
ENDSEC;

DATA;
#10=MECHANICAL_DESIGN_GEOMETRIC_PRESENTATION_REPRESENTATION('',(#895),#23728);
#683=SHAPE_REPRESENTATION_RELATIONSHIP('SRR','None',#24148,#789);
#789=ADVANCED_BREP_SHAPE_REPRESENTATION('',(#1008),#23648);
#895=STYLED_ITEM('',(#24772),#1008);
#1008=MANIFOLD_SOLID_BREP('Body1',#12426);
#1265=FACE_BOUND('',#3124,.T.);
#1626=PLANE('',#14275);
#1627=PLANE('',#14280);
#1628=PLANE('',#14283);
#2168=FACE_OUTER_BOUND('',#3123,.T.);
#2169=FACE_OUTER_BOUND('',#3125,.T.);
#2170=FACE_OUTER_BOUND('',#3126,.T.);
#2171=FACE_OUTER_BOUND('',#3127,.T.);
#2172=FACE_OUTER_BOUND('',#3128,.T.);
#3123=EDGE_LOOP('',(#9505));
#3124=EDGE_LOOP('',(#9506));
#3125=EDGE_LOOP('',(#9507,#9508,#9509,#9510));
#3126=EDGE_LOOP('',(#9511));
#3127=EDGE_LOOP('',(#9512,#9513,#9514,#9515));
#3128=EDGE_LOOP('',(#9516));
#4131=LINE('',#21009,#4806);
#4132=LINE('',#21015,#4807);
#4806=VECTOR('',#16962,0.35);
#4807=VECTOR('',#16971,0.2);
#5483=CIRCLE('',#14276,0.35);
#5484=CIRCLE('',#14277,0.2);
#5485=CIRCLE('',#14279,0.35);
#5486=CIRCLE('',#14282,0.2);
#6333=VERTEX_POINT('',#21003);
#6334=VERTEX_POINT('',#21005);
#6335=VERTEX_POINT('',#21008);
#6336=VERTEX_POINT('',#21013);
#7492=EDGE_CURVE('',#6333,#6333,#5483,.T.);
#7493=EDGE_CURVE('',#6334,#6334,#5484,.T.);
#7494=EDGE_CURVE('',#6333,#6335,#4131,.T.);
#7495=EDGE_CURVE('',#6335,#6335,#5485,.T.);
#7496=EDGE_CURVE('',#6336,#6336,#5486,.T.);
#7497=EDGE_CURVE('',#6336,#6334,#4132,.T.);
#9505=ORIENTED_EDGE('',*,*,#7492,.T.);
#9506=ORIENTED_EDGE('',*,*,#7493,.F.);
#9507=ORIENTED_EDGE('',*,*,#7492,.F.);
#9508=ORIENTED_EDGE('',*,*,#7494,.T.);
#9509=ORIENTED_EDGE('',*,*,#7495,.T.);
#9510=ORIENTED_EDGE('',*,*,#7494,.F.);
#9511=ORIENTED_EDGE('',*,*,#7495,.F.);
#9512=ORIENTED_EDGE('',*,*,#7496,.F.);
#9513=ORIENTED_EDGE('',*,*,#7497,.T.);
#9514=ORIENTED_EDGE('',*,*,#7493,.T.);
#9515=ORIENTED_EDGE('',*,*,#7497,.F.);
#9516=ORIENTED_EDGE('',*,*,#7496,.T.);
#11407=CYLINDRICAL_SURFACE('',#14278,0.35);
#11408=CYLINDRICAL_SURFACE('',#14281,0.2);
#11893=ADVANCED_FACE('',(#2168,#1265),#1626,.T.);
#11894=ADVANCED_FACE('',(#2169),#11407,.T.);
#11895=ADVANCED_FACE('',(#2170),#1627,.F.);
#11896=ADVANCED_FACE('',(#2171),#11408,.T.);
#11897=ADVANCED_FACE('',(#2172),#1628,.T.);
#12426=CLOSED_SHELL('',(#11893,#11894,#11895,#11896,#11897));
#14274=AXIS2_PLACEMENT_3D('',#21001,#16952,#16953);
#14275=AXIS2_PLACEMENT_3D('',#21002,#16954,#16955);
#14276=AXIS2_PLACEMENT_3D('',#21004,#16956,#16957);
#14277=AXIS2_PLACEMENT_3D('',#21006,#16958,#16959);
#14278=AXIS2_PLACEMENT_3D('',#21007,#16960,#16961);
#14279=AXIS2_PLACEMENT_3D('',#21010,#16963,#16964);
#14280=AXIS2_PLACEMENT_3D('',#21011,#16965,#16966);
#14281=AXIS2_PLACEMENT_3D('',#21012,#16967,#16968);
#14282=AXIS2_PLACEMENT_3D('',#21014,#16969,#16970);
#14283=AXIS2_PLACEMENT_3D('',#21016,#16972,#16973);
#16952=DIRECTION('axis',(0.,0.,1.));
#16953=DIRECTION('refdir',(1.,0.,0.));
#16954=DIRECTION('center_axis',(0.,1.,0.));
#16955=DIRECTION('ref_axis',(1.,0.,0.));
#16956=DIRECTION('center_axis',(0.,1.,0.));
#16957=DIRECTION('ref_axis',(1.,0.,0.));
#16958=DIRECTION('center_axis',(0.,1.,0.));
#16959=DIRECTION('ref_axis',(1.,0.,0.));
#16960=DIRECTION('center_axis',(0.,1.,0.));
#16961=DIRECTION('ref_axis',(1.,0.,0.));
#16962=DIRECTION('',(0.,-1.,0.));
#16963=DIRECTION('center_axis',(0.,1.,0.));
#16964=DIRECTION('ref_axis',(1.,0.,0.));
#16965=DIRECTION('center_axis',(0.,1.,0.));
#16966=DIRECTION('ref_axis',(1.,0.,0.));
#16967=DIRECTION('center_axis',(0.,1.,0.));
#16968=DIRECTION('ref_axis',(1.,0.,0.));
#16969=DIRECTION('center_axis',(0.,1.,0.));
#16970=DIRECTION('ref_axis',(1.,0.,0.));
#16971=DIRECTION('',(0.,-1.,0.));
#16972=DIRECTION('center_axis',(0.,1.,0.));
#16973=DIRECTION('ref_axis',(1.,0.,0.));
#21001=CARTESIAN_POINT('',(0.,0.,0.));
#21002=CARTESIAN_POINT('Origin',(-1.30814754519511,-0.8,16.3081475451951));
#21003=CARTESIAN_POINT('',(-1.65814754519511,-0.8,16.3081475451951));
#21004=CARTESIAN_POINT('Origin',(-1.30814754519511,-0.8,16.3081475451951));
#21005=CARTESIAN_POINT('',(-1.50814754519511,-0.8,16.3081475451951));
#21006=CARTESIAN_POINT('Origin',(-1.30814754519511,-0.8,16.3081475451951));
#21007=CARTESIAN_POINT('Origin',(-1.30814754519511,-1.2,16.3081475451951));
#21008=CARTESIAN_POINT('',(-1.65814754519511,-1.2,16.3081475451951));
#21009=CARTESIAN_POINT('',(-1.65814754519511,-1.2,16.3081475451951));
#21010=CARTESIAN_POINT('Origin',(-1.30814754519511,-1.2,16.3081475451951));
#21011=CARTESIAN_POINT('Origin',(-1.30814754519511,-1.2,16.3081475451951));
#21012=CARTESIAN_POINT('Origin',(-1.30814754519511,-0.8,16.3081475451951));
#21013=CARTESIAN_POINT('',(-1.50814754519511,-0.1,16.3081475451951));
#21014=CARTESIAN_POINT('Origin',(-1.30814754519511,-0.1,16.3081475451951));
#21015=CARTESIAN_POINT('',(-1.50814754519511,-0.8,16.3081475451951));
#21016=CARTESIAN_POINT('Origin',(-1.30814754519511,-0.1,16.3081475451951));
#23531=UNCERTAINTY_MEASURE_WITH_UNIT(LENGTH_MEASURE(0.001),#23729,
'DISTANCE_ACCURACY_VALUE',
'Maximum model space distance between geometric entities at asserted c
onnectivities');
#23611=UNCERTAINTY_MEASURE_WITH_UNIT(LENGTH_MEASURE(0.001),#23729,
'DISTANCE_ACCURACY_VALUE',
'Maximum model space distance between geometric entities at asserted c
onnectivities');
#23648=(
GEOMETRIC_REPRESENTATION_CONTEXT(3)
GLOBAL_UNCERTAINTY_ASSIGNED_CONTEXT((#23531))
GLOBAL_UNIT_ASSIGNED_CONTEXT((#23729,#23731,#23732))
REPRESENTATION_CONTEXT('','3D')
);
#23728=(
GEOMETRIC_REPRESENTATION_CONTEXT(3)
GLOBAL_UNCERTAINTY_ASSIGNED_CONTEXT((#23611))
GLOBAL_UNIT_ASSIGNED_CONTEXT((#23729,#23731,#23732))
REPRESENTATION_CONTEXT('','3D')
);
#23729=(
LENGTH_UNIT()
NAMED_UNIT(*)
SI_UNIT(.CENTI.,.METRE.)
);
#23731=(
NAMED_UNIT(*)
PLANE_ANGLE_UNIT()
SI_UNIT($,.RADIAN.)
);
#23732=(
NAMED_UNIT(*)
SI_UNIT($,.STERADIAN.)
SOLID_ANGLE_UNIT()
);
#23769=SHAPE_DEFINITION_REPRESENTATION(#23885,#24148);
#23885=PRODUCT_DEFINITION_SHAPE('',$,#24265);
#24148=SHAPE_REPRESENTATION('',(#14274),#23648);
#24228=PRODUCT_DEFINITION_CONTEXT('part definition',#24578,'design');
#24265=PRODUCT_DEFINITION('M4 short cap screw (1)',
'M4 short cap screw (1)',#24381,#24228);
#24381=PRODUCT_DEFINITION_FORMATION('',$,#24616);
#24578=APPLICATION_CONTEXT(
'Core Data for Automotive Mechanical Design Process');
#24579=PRODUCT_CONTEXT('part definition',#24578,'mechanical');
#24616=PRODUCT('M4 short cap screw (1)','M4 short cap screw (1)',
'M4 short cap screw (1)',(#24579));
#24766=COLOUR_RGB('Black',0.12,0.14,0.17);
#24767=FILL_AREA_STYLE_COLOUR('',#24766);
#24768=FILL_AREA_STYLE('',(#24767));
#24769=SURFACE_STYLE_FILL_AREA(#24768);
#24770=SURFACE_SIDE_STYLE('',(#24769));
#24771=SURFACE_STYLE_USAGE(.BOTH.,#24770);
#24772=PRESENTATION_STYLE_ASSIGNMENT((#24771));
ENDSEC;
END-ISO-10303-21;
